ISO-10303-21;
HEADER;
/* Generated by software containing ST-Developer
 * from STEP Tools, Inc. (www.steptools.com) 
 */

FILE_DESCRIPTION(
/* description */ (''),
/* implementation_level */ '2;1');

FILE_NAME(
/* name */ 'Cap_Screw_01.step',
/* time_stamp */ '2026-10-22T13:39:42+06:00',
/* author */ (''),
/* organization */ (''),
/* preprocessor_version */ 'ST-DEVELOPER v20.2',
/* originating_system */ 'Autodesk Translation Framework v15.15.0.0',
/* authorisation */ '');

FILE_SCHEMA (('AUTOMOTIVE_DESIGN { 1 0 10303 214 3 1 1 }'));
ENDSEC;

DATA;
#10=MECHANICAL_DESIGN_GEOMETRIC_PRESENTATION_REPRESENTATION('',(#307),#17836);
#287=SHAPE_REPRESENTATION_RELATIONSHIP('SRR','None',#17874,#297);
#297=ADVANCED_BREP_SHAPE_REPRESENTATION('',(#317),#17826);
#307=STYLED_ITEM('',(#17980),#317);
#317=MANIFOLD_SOLID_BREP('Cap_Screw_01',#9628);
#327=CYLINDRICAL_SURFACE('',#9757,9.);
#328=CYLINDRICAL_SURFACE('',#9761,7.5);
#640=LINE('',#14274,#1305);
#641=LINE('',#14278,#1306);
#642=LINE('',#14282,#1307);
#643=LINE('',#14285,#1308);
#1305=VECTOR('',#11046,8.5);
#1306=VECTOR('',#11051,9.);
#1307=VECTOR('',#11058,8.5);
#1308=VECTOR('',#11061,7.5);
#1970=CONICAL_SURFACE('',#9754,8.5,0.78539816339745);
#1971=CONICAL_SURFACE('',#9760,8.5,0.78539816339745);
#1974=FACE_BOUND('',#2642,.T.);
#2027=FACE_OUTER_BOUND('',#2641,.T.);
#2028=FACE_OUTER_BOUND('',#2643,.T.);
#2029=FACE_OUTER_BOUND('',#2644,.T.);
#2030=FACE_OUTER_BOUND('',#2645,.T.);
#2031=FACE_OUTER_BOUND('',#2646,.T.);
#2032=FACE_OUTER_BOUND('',#2647,.T.);
#2033=FACE_OUTER_BOUND('',#2648,.T.);
#2641=EDGE_LOOP('',(#6103));
#2642=EDGE_LOOP('',(#6104));
#2643=EDGE_LOOP('',(#6105,#6106,#6107,#6108));
#2644=EDGE_LOOP('',(#6109,#6110,#6111,#6112));
#2645=EDGE_LOOP('',(#6113));
#2646=EDGE_LOOP('',(#6114,#6115,#6116,#6117));
#2647=EDGE_LOOP('',(#6118,#6119,#6120,#6121));
#2648=EDGE_LOOP('',(#6122));
#3308=CIRCLE('',#9752,8.);
#3309=CIRCLE('',#9753,7.5);
#3310=CIRCLE('',#9755,8.);
#3311=CIRCLE('',#9756,9.);
#3312=CIRCLE('',#9758,9.);
#3313=CIRCLE('',#9762,7.5);
#3936=VERTEX_POINT('',#14266);
#3937=VERTEX_POINT('',#14268);
#3938=VERTEX_POINT('',#14271);
#3939=VERTEX_POINT('',#14273);
#3940=VERTEX_POINT('',#14277);
#3941=VERTEX_POINT('',#14284);
#4722=EDGE_CURVE('',#3936,#3936,#3308,.T.);
#4723=EDGE_CURVE('',#3937,#3937,#3309,.T.);
#4724=EDGE_CURVE('',#3938,#3938,#3310,.T.);
#4725=EDGE_CURVE('',#3938,#3939,#640,.T.);
#4726=EDGE_CURVE('',#3939,#3939,#3311,.T.);
#4727=EDGE_CURVE('',#3939,#3940,#641,.T.);
#4728=EDGE_CURVE('',#3940,#3940,#3312,.T.);
#4729=EDGE_CURVE('',#3940,#3936,#642,.T.);
#4730=EDGE_CURVE('',#3937,#3941,#643,.T.);
#4731=EDGE_CURVE('',#3941,#3941,#3313,.T.);
#6103=ORIENTED_EDGE('',*,*,#4722,.F.);
#6104=ORIENTED_EDGE('',*,*,#4723,.T.);
#6105=ORIENTED_EDGE('',*,*,#4724,.T.);
#6106=ORIENTED_EDGE('',*,*,#4725,.T.);
#6107=ORIENTED_EDGE('',*,*,#4726,.T.);
#6108=ORIENTED_EDGE('',*,*,#4725,.F.);
#6109=ORIENTED_EDGE('',*,*,#4726,.F.);
#6110=ORIENTED_EDGE('',*,*,#4727,.T.);
#6111=ORIENTED_EDGE('',*,*,#4728,.F.);
#6112=ORIENTED_EDGE('',*,*,#4727,.F.);
#6113=ORIENTED_EDGE('',*,*,#4724,.F.);
#6114=ORIENTED_EDGE('',*,*,#4728,.T.);
#6115=ORIENTED_EDGE('',*,*,#4729,.T.);
#6116=ORIENTED_EDGE('',*,*,#4722,.T.);
#6117=ORIENTED_EDGE('',*,*,#4729,.F.);
#6118=ORIENTED_EDGE('',*,*,#4723,.F.);
#6119=ORIENTED_EDGE('',*,*,#4730,.T.);
#6120=ORIENTED_EDGE('',*,*,#4731,.T.);
#6121=ORIENTED_EDGE('',*,*,#4730,.F.);
#6122=ORIENTED_EDGE('',*,*,#4731,.F.);
#8865=PLANE('',#9751);
#8866=PLANE('',#9759);
#8867=PLANE('',#9763);
#9014=ADVANCED_FACE('',(#2027,#1974),#8865,.F.);
#9015=ADVANCED_FACE('',(#2028),#1970,.T.);
#9016=ADVANCED_FACE('',(#2029),#327,.T.);
#9017=ADVANCED_FACE('',(#2030),#8866,.T.);
#9018=ADVANCED_FACE('',(#2031),#1971,.T.);
#9019=ADVANCED_FACE('',(#2032),#328,.T.);
#9020=ADVANCED_FACE('',(#2033),#8867,.F.);
#9628=CLOSED_SHELL('',(#9014,#9015,#9016,#9017,#9018,#9019,#9020));
#9750=AXIS2_PLACEMENT_3D('',#14264,#11034,#11035);
#9751=AXIS2_PLACEMENT_3D('',#14265,#11036,#11037);
#9752=AXIS2_PLACEMENT_3D('',#14267,#11038,#11039);
#9753=AXIS2_PLACEMENT_3D('',#14269,#11040,#11041);
#9754=AXIS2_PLACEMENT_3D('',#14270,#11042,#11043);
#9755=AXIS2_PLACEMENT_3D('',#14272,#11044,#11045);
#9756=AXIS2_PLACEMENT_3D('',#14275,#11047,#11048);
#9757=AXIS2_PLACEMENT_3D('',#14276,#11049,#11050);
#9758=AXIS2_PLACEMENT_3D('',#14279,#11052,#11053);
#9759=AXIS2_PLACEMENT_3D('',#14280,#11054,#11055);
#9760=AXIS2_PLACEMENT_3D('',#14281,#11056,#11057);
#9761=AXIS2_PLACEMENT_3D('',#14283,#11059,#11060);
#9762=AXIS2_PLACEMENT_3D('',#14286,#11062,#11063);
#9763=AXIS2_PLACEMENT_3D('',#14287,#11064,#11065);
#11034=DIRECTION('axis',(0.,0.,1.));
#11035=DIRECTION('refdir',(1.,0.,0.));
#11036=DIRECTION('center_axis',(0.,-1.,0.));
#11037=DIRECTION('ref_axis',(1.,0.,0.));
#11038=DIRECTION('center_axis',(0.,-1.,0.));
#11039=DIRECTION('ref_axis',(1.,0.,0.));
#11040=DIRECTION('center_axis',(0.,-1.,0.));
#11041=DIRECTION('ref_axis',(1.,0.,0.));
#11042=DIRECTION('center_axis',(0.,1.,0.));
#11043=DIRECTION('ref_axis',(1.,0.,0.));
#11044=DIRECTION('center_axis',(0.,1.,0.));
#11045=DIRECTION('ref_axis',(1.,0.,0.));
#11046=DIRECTION('',(-0.707106781186549,0.707106781186546,-8.65956056235495E-17));
#11047=DIRECTION('center_axis',(0.,-1.,0.));
#11048=DIRECTION('ref_axis',(1.,0.,0.));
#11049=DIRECTION('center_axis',(0.,-1.,0.));
#11050=DIRECTION('ref_axis',(1.,0.,0.));
#11051=DIRECTION('',(0.,1.,0.));
#11052=DIRECTION('center_axis',(0.,1.,0.));
#11053=DIRECTION('ref_axis',(1.,0.,0.));
#11054=DIRECTION('center_axis',(0.,-1.,0.));
#11055=DIRECTION('ref_axis',(1.,0.,0.));
#11056=DIRECTION('center_axis',(0.,-1.,0.));
#11057=DIRECTION('ref_axis',(1.,0.,0.));
#11058=DIRECTION('',(0.707106781186549,0.707106781186546,8.65956056235495E-17));
#11059=DIRECTION('center_axis',(0.,-1.,0.));
#11060=DIRECTION('ref_axis',(1.,0.,0.));
#11061=DIRECTION('',(0.,1.,0.));
#11062=DIRECTION('center_axis',(0.,-1.,0.));
#11063=DIRECTION('ref_axis',(1.,0.,0.));
#11064=DIRECTION('center_axis',(0.,-1.,0.));
#11065=DIRECTION('ref_axis',(1.,0.,0.));
#14264=CARTESIAN_POINT('',(0.,0.,0.));
#14265=CARTESIAN_POINT('Origin',(0.,-115.,16.0775024873567));
#14266=CARTESIAN_POINT('',(-8.,-115.,16.0775024873567));
#14267=CARTESIAN_POINT('Origin',(0.,-115.,16.0775024873567));
#14268=CARTESIAN_POINT('',(-7.5,-115.,16.0775024873567));
#14269=CARTESIAN_POINT('Origin',(0.,-115.,16.0775024873567));
#14270=CARTESIAN_POINT('Origin',(0.,-134.5,16.0775024873567));
#14271=CARTESIAN_POINT('',(-8.,-135.,16.0775024873567));
#14272=CARTESIAN_POINT('Origin',(0.,-135.,16.0775024873567));
#14273=CARTESIAN_POINT('',(-9.,-134.,16.0775024873567));
#14274=CARTESIAN_POINT('',(-8.5,-134.5,16.0775024873567));
#14275=CARTESIAN_POINT('Origin',(0.,-134.,16.0775024873567));
#14276=CARTESIAN_POINT('Origin',(0.,-115.,16.0775024873567));
#14277=CARTESIAN_POINT('',(-9.,-116.,16.0775024873567));
#14278=CARTESIAN_POINT('',(-9.,-115.,16.0775024873567));
#14279=CARTESIAN_POINT('Origin',(0.,-116.,16.0775024873567));
#14280=CARTESIAN_POINT('Origin',(0.,-135.,16.0775024873567));
#14281=CARTESIAN_POINT('Origin',(0.,-115.5,16.0775024873567));
#14282=CARTESIAN_POINT('',(-8.5,-115.5,16.0775024873567));
#14283=CARTESIAN_POINT('Origin',(0.,-90.,16.0775024873567));
#14284=CARTESIAN_POINT('',(-7.5,-90.,16.0775024873567));
#14285=CARTESIAN_POINT('',(-7.5,-90.,16.0775024873567));
#14286=CARTESIAN_POINT('Origin',(0.,-90.,16.0775024873567));
#14287=CARTESIAN_POINT('Origin',(0.,-90.,16.0775024873567));
#17814=UNCERTAINTY_MEASURE_WITH_UNIT(LENGTH_MEASURE(0.01),#17837,
'DISTANCE_ACCURACY_VALUE',
'Maximum model space distance between geometric entities at asserted c
onnectivities');
#17824=UNCERTAINTY_MEASURE_WITH_UNIT(LENGTH_MEASURE(0.01),#17837,
'DISTANCE_ACCURACY_VALUE',
'Maximum model space distance between geometric entities at asserted c
onnectivities');
#17826=(
GEOMETRIC_REPRESENTATION_CONTEXT(3)
GLOBAL_UNCERTAINTY_ASSIGNED_CONTEXT((#17814))
GLOBAL_UNIT_ASSIGNED_CONTEXT((#17837,#17839,#17840))
REPRESENTATION_CONTEXT('','3D')
);
#17836=(
GEOMETRIC_REPRESENTATION_CONTEXT(3)
GLOBAL_UNCERTAINTY_ASSIGNED_CONTEXT((#17824))
GLOBAL_UNIT_ASSIGNED_CONTEXT((#17837,#17839,#17840))
REPRESENTATION_CONTEXT('','3D')
);
#17837=(
LENGTH_UNIT()
NAMED_UNIT(*)
SI_UNIT(.MILLI.,.METRE.)
);
#17839=(
NAMED_UNIT(*)
PLANE_ANGLE_UNIT()
SI_UNIT($,.RADIAN.)
);
#17840=(
NAMED_UNIT(*)
SI_UNIT($,.STERADIAN.)
SOLID_ANGLE_UNIT()
);
#17842=SHAPE_DEFINITION_REPRESENTATION(#17853,#17874);
#17853=PRODUCT_DEFINITION_SHAPE('',$,#17886);
#17874=SHAPE_REPRESENTATION('',(#9750),#17826);
#17884=PRODUCT_DEFINITION_CONTEXT('part definition',#17919,'design');
#17886=PRODUCT_DEFINITION('Cap_Screw_01','Cap_Screw_01',#17897,#17884);
#17897=PRODUCT_DEFINITION_FORMATION('',$,#17922);
#17919=APPLICATION_CONTEXT(
'Core Data for Automotive Mechanical Design Process');
#17920=PRODUCT_CONTEXT('part definition',#17919,'mechanical');
#17922=PRODUCT('Cap_Screw_01','Cap_Screw_01',$,(#17920));
#17974=COLOUR_RGB('Black',0.12,0.14,0.17);
#17975=FILL_AREA_STYLE_COLOUR('',#17974);
#17976=FILL_AREA_STYLE('',(#17975));
#17977=SURFACE_STYLE_FILL_AREA(#17976);
#17978=SURFACE_SIDE_STYLE('',(#17977));
#17979=SURFACE_STYLE_USAGE(.BOTH.,#17978);
#17980=PRESENTATION_STYLE_ASSIGNMENT((#17979));
ENDSEC;
END-ISO-10303-21;
